ISO-10303-21;
HEADER;
/* Generated by software containing ST-Developer
 * from STEP Tools, Inc. (www.steptools.com) 
 */

FILE_DESCRIPTION(
/* description */ ('CAx-IF Rec.Pracs.---Representation and Presentation of Product Manufa
cturing Information (PMI)---4.0---2014-10-13'),
/* implementation_level */ '2;1');

FILE_NAME(
/* name */ 'Socket Screw 1.step',
/* time_stamp */ '2026-10-24T18:52:33-07:00',
/* author */ (''),
/* organization */ (''),
/* preprocessor_version */ 'ST-DEVELOPER v20.2',
/* originating_system */ 'Autodesk Translation Framework v15.17.0.0',
/* authorisation */ '');

FILE_SCHEMA (('AP242_MANAGED_MODEL_BASED_3D_ENGINEERING_MIM_LF { 1 0 10303 442 2 1 4 }'));
ENDSEC;

DATA;
#10=MECHANICAL_DESIGN_GEOMETRIC_PRESENTATION_REPRESENTATION('',(#421),#34876);
#355=SHAPE_REPRESENTATION_RELATIONSHIP('SRR','None',#34992,#388);
#388=ADVANCED_BREP_SHAPE_REPRESENTATION('',(#454),#34850);
#421=STYLED_ITEM('',(#35164),#454);
#454=MANIFOLD_SOLID_BREP('Socket Screw 1',#19561);
#778=PLANE('',#20810);
#779=PLANE('',#20811);
#780=PLANE('',#20815);
#781=PLANE('',#20816);
#782=PLANE('',#20817);
#783=PLANE('',#20818);
#784=PLANE('',#20819);
#785=PLANE('',#20820);
#1639=LINE('',#30892,#3238);
#1640=LINE('',#30894,#3239);
#1641=LINE('',#30896,#3240);
#1642=LINE('',#30897,#3241);
#1643=LINE('',#30900,#3242);
#1644=LINE('',#30902,#3243);
#1645=LINE('',#30903,#3244);
#1646=LINE('',#30907,#3245);
#1647=LINE('',#30911,#3246);
#1648=LINE('',#30914,#3247);
#1649=LINE('',#30915,#3248);
#1650=LINE('',#30918,#3249);
#1651=LINE('',#30920,#3250);
#1652=LINE('',#30921,#3251);
#1653=LINE('',#30924,#3252);
#1654=LINE('',#30925,#3253);
#1655=LINE('',#30928,#3254);
#1656=LINE('',#30929,#3255);
#1657=LINE('',#30931,#3256);
#3238=VECTOR('',#24534,1.);
#3239=VECTOR('',#24535,1.);
#3240=VECTOR('',#24536,1.);
#3241=VECTOR('',#24537,1.);
#3242=VECTOR('',#24540,1.);
#3243=VECTOR('',#24541,1.);
#3244=VECTOR('',#24542,1.);
#3245=VECTOR('',#24545,1.);
#3246=VECTOR('',#24548,1.);
#3247=VECTOR('',#24553,1.);
#3248=VECTOR('',#24554,1.);
#3249=VECTOR('',#24557,1.);
#3250=VECTOR('',#24558,1.);
#3251=VECTOR('',#24559,1.);
#3252=VECTOR('',#24562,1.);
#3253=VECTOR('',#24563,1.);
#3254=VECTOR('',#24566,1.);
#3255=VECTOR('',#24567,1.);
#3256=VECTOR('',#24570,1.);
#4466=CYLINDRICAL_SURFACE('',#20812,0.0005);
#5176=FACE_OUTER_BOUND('',#6260,.T.);
#5177=FACE_OUTER_BOUND('',#6261,.T.);
#5178=FACE_OUTER_BOUND('',#6262,.T.);
#5179=FACE_OUTER_BOUND('',#6263,.T.);
#5180=FACE_OUTER_BOUND('',#6264,.T.);
#5181=FACE_OUTER_BOUND('',#6265,.T.);
#5182=FACE_OUTER_BOUND('',#6266,.T.);
#5183=FACE_OUTER_BOUND('',#6267,.T.);
#5184=FACE_OUTER_BOUND('',#6268,.T.);
#6260=EDGE_LOOP('',(#14892,#14893,#14894,#14895));
#6261=EDGE_LOOP('',(#14896,#14897,#14898,#14899));
#6262=EDGE_LOOP('',(#14900,#14901,#14902,#14903));
#6263=EDGE_LOOP('',(#14904,#14905,#14906,#14907));
#6264=EDGE_LOOP('',(#14908,#14909,#14910,#14911,#14912,#14913,#14914));
#6265=EDGE_LOOP('',(#14915,#14916,#14917,#14918));
#6266=EDGE_LOOP('',(#14919,#14920,#14921,#14922,#14923,#14924,#14925));
#6267=EDGE_LOOP('',(#14926,#14927,#14928,#14929));
#6268=EDGE_LOOP('',(#14930,#14931,#14932,#14933));
#7372=CIRCLE('',#20813,0.00050000000001);
#7373=CIRCLE('',#20814,0.00050000000001);
#8764=VERTEX_POINT('',#30890);
#8765=VERTEX_POINT('',#30891);
#8766=VERTEX_POINT('',#30893);
#8767=VERTEX_POINT('',#30895);
#8768=VERTEX_POINT('',#30899);
#8769=VERTEX_POINT('',#30901);
#8770=VERTEX_POINT('',#30905);
#8771=VERTEX_POINT('',#30906);
#8772=VERTEX_POINT('',#30908);
#8773=VERTEX_POINT('',#30910);
#8774=VERTEX_POINT('',#30917);
#8775=VERTEX_POINT('',#30919);
#8776=VERTEX_POINT('',#30923);
#8777=VERTEX_POINT('',#30927);
#11004=EDGE_CURVE('',#8764,#8765,#1639,.T.);
#11005=EDGE_CURVE('',#8766,#8765,#1640,.T.);
#11006=EDGE_CURVE('',#8766,#8767,#1641,.T.);
#11007=EDGE_CURVE('',#8764,#8767,#1642,.T.);
#11008=EDGE_CURVE('',#8768,#8766,#1643,.T.);
#11009=EDGE_CURVE('',#8769,#8768,#1644,.T.);
#11010=EDGE_CURVE('',#8767,#8769,#1645,.T.);
#11011=EDGE_CURVE('',#8770,#8771,#1646,.T.);
#11012=EDGE_CURVE('',#8770,#8772,#7372,.T.);
#11013=EDGE_CURVE('',#8772,#8773,#1647,.T.);
#11014=EDGE_CURVE('',#8771,#8773,#7373,.T.);
#11015=EDGE_CURVE('',#8772,#8769,#1648,.T.);
#11016=EDGE_CURVE('',#8773,#8768,#1649,.T.);
#11017=EDGE_CURVE('',#8774,#8770,#1650,.T.);
#11018=EDGE_CURVE('',#8775,#8774,#1651,.T.);
#11019=EDGE_CURVE('',#8764,#8775,#1652,.T.);
#11020=EDGE_CURVE('',#8776,#8775,#1653,.T.);
#11021=EDGE_CURVE('',#8765,#8776,#1654,.T.);
#11022=EDGE_CURVE('',#8777,#8776,#1655,.T.);
#11023=EDGE_CURVE('',#8771,#8777,#1656,.T.);
#11024=EDGE_CURVE('',#8774,#8777,#1657,.T.);
#14892=ORIENTED_EDGE('',*,*,#11004,.T.);
#14893=ORIENTED_EDGE('',*,*,#11005,.F.);
#14894=ORIENTED_EDGE('',*,*,#11006,.T.);
#14895=ORIENTED_EDGE('',*,*,#11007,.F.);
#14896=ORIENTED_EDGE('',*,*,#11006,.F.);
#14897=ORIENTED_EDGE('',*,*,#11008,.F.);
#14898=ORIENTED_EDGE('',*,*,#11009,.F.);
#14899=ORIENTED_EDGE('',*,*,#11010,.F.);
#14900=ORIENTED_EDGE('',*,*,#11011,.F.);
#14901=ORIENTED_EDGE('',*,*,#11012,.T.);
#14902=ORIENTED_EDGE('',*,*,#11013,.T.);
#14903=ORIENTED_EDGE('',*,*,#11014,.F.);
#14904=ORIENTED_EDGE('',*,*,#11013,.F.);
#14905=ORIENTED_EDGE('',*,*,#11015,.T.);
#14906=ORIENTED_EDGE('',*,*,#11009,.T.);
#14907=ORIENTED_EDGE('',*,*,#11016,.F.);
#14908=ORIENTED_EDGE('',*,*,#11017,.F.);
#14909=ORIENTED_EDGE('',*,*,#11018,.F.);
#14910=ORIENTED_EDGE('',*,*,#11019,.F.);
#14911=ORIENTED_EDGE('',*,*,#11007,.T.);
#14912=ORIENTED_EDGE('',*,*,#11010,.T.);
#14913=ORIENTED_EDGE('',*,*,#11015,.F.);
#14914=ORIENTED_EDGE('',*,*,#11012,.F.);
#14915=ORIENTED_EDGE('',*,*,#11019,.T.);
#14916=ORIENTED_EDGE('',*,*,#11020,.F.);
#14917=ORIENTED_EDGE('',*,*,#11021,.F.);
#14918=ORIENTED_EDGE('',*,*,#11004,.F.);
#14919=ORIENTED_EDGE('',*,*,#11021,.T.);
#14920=ORIENTED_EDGE('',*,*,#11022,.F.);
#14921=ORIENTED_EDGE('',*,*,#11023,.F.);
#14922=ORIENTED_EDGE('',*,*,#11014,.T.);
#14923=ORIENTED_EDGE('',*,*,#11016,.T.);
#14924=ORIENTED_EDGE('',*,*,#11008,.T.);
#14925=ORIENTED_EDGE('',*,*,#11005,.T.);
#14926=ORIENTED_EDGE('',*,*,#11023,.T.);
#14927=ORIENTED_EDGE('',*,*,#11024,.F.);
#14928=ORIENTED_EDGE('',*,*,#11017,.T.);
#14929=ORIENTED_EDGE('',*,*,#11011,.T.);
#14930=ORIENTED_EDGE('',*,*,#11024,.T.);
#14931=ORIENTED_EDGE('',*,*,#11022,.T.);
#14932=ORIENTED_EDGE('',*,*,#11020,.T.);
#14933=ORIENTED_EDGE('',*,*,#11018,.T.);
#18892=ADVANCED_FACE('',(#5176),#778,.T.);
#18893=ADVANCED_FACE('',(#5177),#779,.F.);
#18894=ADVANCED_FACE('',(#5178),#4466,.T.);
#18895=ADVANCED_FACE('',(#5179),#780,.F.);
#18896=ADVANCED_FACE('',(#5180),#781,.T.);
#18897=ADVANCED_FACE('',(#5181),#782,.T.);
#18898=ADVANCED_FACE('',(#5182),#783,.T.);
#18899=ADVANCED_FACE('',(#5183),#784,.T.);
#18900=ADVANCED_FACE('',(#5184),#785,.T.);
#19561=CLOSED_SHELL('',(#18892,#18893,#18894,#18895,#18896,#18897,#18898,
#18899,#18900));
#20809=AXIS2_PLACEMENT_3D('',#30888,#24530,#24531);
#20810=AXIS2_PLACEMENT_3D('',#30889,#24532,#24533);
#20811=AXIS2_PLACEMENT_3D('',#30898,#24538,#24539);
#20812=AXIS2_PLACEMENT_3D('',#30904,#24543,#24544);
#20813=AXIS2_PLACEMENT_3D('',#30909,#24546,#24547);
#20814=AXIS2_PLACEMENT_3D('',#30912,#24549,#24550);
#20815=AXIS2_PLACEMENT_3D('',#30913,#24551,#24552);
#20816=AXIS2_PLACEMENT_3D('',#30916,#24555,#24556);
#20817=AXIS2_PLACEMENT_3D('',#30922,#24560,#24561);
#20818=AXIS2_PLACEMENT_3D('',#30926,#24564,#24565);
#20819=AXIS2_PLACEMENT_3D('',#30930,#24568,#24569);
#20820=AXIS2_PLACEMENT_3D('',#30932,#24571,#24572);
#24530=DIRECTION('axis',(0.,0.,1.));
#24531=DIRECTION('refdir',(1.,0.,0.));
#24532=DIRECTION('center_axis',(1.,5.1420277733694E-16,-1.0522467400333E-14));
#24533=DIRECTION('ref_axis',(-1.0522467400333E-14,1.06077175752244E-14,
-1.));
#24534=DIRECTION('',(-1.00001914094642E-12,1.00002200370999E-12,1.));
#24535=DIRECTION('',(9.99479153109778E-13,1.,-9.99999999999011E-13));
#24536=DIRECTION('',(1.00001914094642E-12,-9.99999999998997E-13,-1.));
#24537=DIRECTION('',(-9.47915311079142E-15,-1.,1.E-14));
#24538=DIRECTION('center_axis',(-4.5961454925099E-16,1.,6.61092274672771E-17));
#24539=DIRECTION('ref_axis',(-1.05885766278003E-14,6.61092274672722E-17,
-1.));
#24540=DIRECTION('',(1.,-9.54038545074888E-15,9.9999999999998E-15));
#24541=DIRECTION('',(-9.56631913100564E-15,9.99999999999985E-15,1.));
#24542=DIRECTION('',(-1.,9.54038545074888E-15,-9.9999999999998E-15));
#24543=DIRECTION('center_axis',(0.,-4.29362650667545E-31,1.));
#24544=DIRECTION('ref_axis',(4.28756753891971E-16,-1.,-4.29362650667545E-31));
#24545=DIRECTION('',(-9.99999999999976E-15,-1.04336808689941E-14,1.));
#24546=DIRECTION('center_axis',(-1.99999999991998E-11,2.E-11,1.));
#24547=DIRECTION('ref_axis',(-1.99995712428458E-11,-1.,1.99999999996E-11));
#24548=DIRECTION('',(-9.56631913100564E-15,9.99999999999985E-15,1.));
#24549=DIRECTION('center_axis',(-1.99999999991998E-11,2.E-11,1.));
#24550=DIRECTION('ref_axis',(-1.99995712428458E-11,-1.,1.99999999996E-11));
#24551=DIRECTION('center_axis',(1.,5.2084688920845E-16,-1.0522467400333E-14));
#24552=DIRECTION('ref_axis',(-1.0522467400333E-14,1.01548957588061E-14,
-1.));
#24553=DIRECTION('',(-9.47915311079142E-15,-1.,1.E-14));
#24554=DIRECTION('',(-9.47915311079142E-15,-1.,1.E-14));
#24555=DIRECTION('center_axis',(-1.0522467400333E-14,-2.20037109949262E-17,
-1.));
#24556=DIRECTION('ref_axis',(1.,-6.86759532082262E-15,-1.0522467400333E-14));
#24557=DIRECTION('',(-1.,9.99485333130104E-13,-9.99628143109513E-13));
#24558=DIRECTION('',(9.99479153109778E-13,1.,-1.00002200371E-12));
#24559=DIRECTION('',(1.,-9.99466108488984E-13,1.00024333162532E-12));
#24560=DIRECTION('center_axis',(5.33891510011771E-16,-1.,2.20037109950003E-17));
#24561=DIRECTION('ref_axis',(-1.,-5.33891510011771E-16,1.0522467400333E-14));
#24562=DIRECTION('',(9.99999999998993E-13,-1.00002200370999E-12,-1.));
#24563=DIRECTION('',(1.,-9.99466108488984E-13,1.00024333162532E-12));
#24564=DIRECTION('center_axis',(-2.43331626335201E-16,2.20037109950001E-17,
1.));
#24565=DIRECTION('ref_axis',(1.,3.89820370584558E-15,2.43331626335201E-16));
#24566=DIRECTION('',(-9.99479153109778E-13,-1.,1.00002200371E-12));
#24567=DIRECTION('',(1.,-9.99466108488984E-13,1.00024333162532E-12));
#24568=DIRECTION('center_axis',(-5.3389151001177E-16,1.,6.61092274672778E-17));
#24569=DIRECTION('ref_axis',(-1.06105803387953E-14,6.61092274672721E-17,
-1.));
#24570=DIRECTION('',(-9.99999999998993E-13,1.00002200370999E-12,1.));
#24571=DIRECTION('center_axis',(1.,5.33891510011885E-16,-1.0522467400333E-14));
#24572=DIRECTION('ref_axis',(-1.0522467400333E-14,1.08319082541355E-14,
-1.));
#30888=CARTESIAN_POINT('',(0.,0.,0.));
#30889=CARTESIAN_POINT('Origin',(0.02115,-0.0223,-0.01175));
#30890=CARTESIAN_POINT('',(0.02115,-0.02545,0.00474999999999993));
#30891=CARTESIAN_POINT('',(0.02115,-0.02545,0.00524999999999993));
#30892=CARTESIAN_POINT('',(0.02115000000001,-0.02545000000001,-0.00349999999999003));
#30893=CARTESIAN_POINT('',(0.02115,-0.0317,0.00524999999999993));
#30894=CARTESIAN_POINT('',(0.0211500000000101,-0.02422500000001,0.00525000000000993));
#30895=CARTESIAN_POINT('',(0.02115,-0.0317,0.00474999999999993));
#30896=CARTESIAN_POINT('',(0.0211500000000101,-0.0317000000000099,-0.00549999999999003));
#30897=CARTESIAN_POINT('',(0.0211500000000101,-0.02545000000001,0.00475000000000993));
#30898=CARTESIAN_POINT('Origin',(0.02115,-0.0317,0.000749999999999928));
#30899=CARTESIAN_POINT('',(0.02065,-0.0317,0.00524999999999993));
#30900=CARTESIAN_POINT('',(0.0206500000000101,-0.03170000000001,0.00525000000000993));
#30901=CARTESIAN_POINT('',(0.02065,-0.0317,0.00474999999999993));
#30902=CARTESIAN_POINT('',(0.0206500000000101,-0.03170000000001,0.00525000000000993));
#30903=CARTESIAN_POINT('',(0.0206500000000101,-0.03170000000001,0.00475000000000993));
#30904=CARTESIAN_POINT('Origin',(0.02115,-0.02545,0.00499999999999993));
#30905=CARTESIAN_POINT('',(0.02115,-0.02495,0.00474999999999993));
#30906=CARTESIAN_POINT('',(0.02115,-0.02495,0.00524999999999993));
#30907=CARTESIAN_POINT('',(0.02115000000001,-0.02495000000001,0.00525000000000993));
#30908=CARTESIAN_POINT('',(0.02065,-0.02545,0.00474999999999993));
#30909=CARTESIAN_POINT('Origin',(0.0211500000000101,-0.02545000000001,0.00475000000000993));
#30910=CARTESIAN_POINT('',(0.02065,-0.02545,0.00524999999999993));
#30911=CARTESIAN_POINT('',(0.0206500000000101,-0.02545000000001,0.00525000000000993));
#30912=CARTESIAN_POINT('Origin',(0.02115000000001,-0.02545000000001,0.00525000000000993));
#30913=CARTESIAN_POINT('Origin',(0.02065,-0.02545,0.00524999999999993));
#30914=CARTESIAN_POINT('',(0.0206500000000101,-0.02545000000001,0.00475000000000993));
#30915=CARTESIAN_POINT('',(0.0206500000000101,-0.02545000000001,0.00525000000000993));
#30916=CARTESIAN_POINT('Origin',(0.0229,-0.02545,0.00474999999999991));
#30917=CARTESIAN_POINT('',(0.0262,-0.02495,0.00474999999999988));
#30918=CARTESIAN_POINT('',(0.0229000000000101,-0.02495000000001,0.00475000000000991));
#30919=CARTESIAN_POINT('',(0.0262,-0.02545,0.00474999999999988));
#30920=CARTESIAN_POINT('',(0.0262000000000101,-0.02495000000001,0.00475000000000998));
#30921=CARTESIAN_POINT('',(0.0229000000000101,-0.02545000000001,0.00475000000000991));
#30922=CARTESIAN_POINT('Origin',(0.0229,-0.02545,0.00524999999999991));
#30923=CARTESIAN_POINT('',(0.0262,-0.02545,0.00524999999999988));
#30924=CARTESIAN_POINT('',(0.0262000000000101,-0.02545000000001,0.00475000000000998));
#30925=CARTESIAN_POINT('',(0.0229000000000101,-0.02545000000001,0.00525000000000991));
#30926=CARTESIAN_POINT('Origin',(0.0229,-0.02495,0.00524999999999991));
#30927=CARTESIAN_POINT('',(0.0262,-0.02495,0.00524999999999988));
#30928=CARTESIAN_POINT('',(0.0262000000000101,-0.02545000000001,0.00525000000000998));
#30929=CARTESIAN_POINT('',(0.0229000000000101,-0.02495000000001,0.00525000000000991));
#30930=CARTESIAN_POINT('Origin',(0.0229,-0.02495,0.00474999999999991));
#30931=CARTESIAN_POINT('',(0.0262000000000101,-0.02495000000001,0.00525000000000998));
#30932=CARTESIAN_POINT('Origin',(0.0262,-0.0252,0.00499999999999988));
#34815=UNCERTAINTY_MEASURE_WITH_UNIT(LENGTH_MEASURE(1.E-5),#34877,
'DISTANCE_ACCURACY_VALUE',
'Maximum model space distance between geometric entities at asserted c
onnectivities');
#34841=UNCERTAINTY_MEASURE_WITH_UNIT(LENGTH_MEASURE(1.E-5),#34877,
'DISTANCE_ACCURACY_VALUE',
'Maximum model space distance between geometric entities at asserted c
onnectivities');
#34850=(
GEOMETRIC_REPRESENTATION_CONTEXT(3)
GLOBAL_UNCERTAINTY_ASSIGNED_CONTEXT((#34815))
GLOBAL_UNIT_ASSIGNED_CONTEXT((#34877,#34878,#34879))
REPRESENTATION_CONTEXT('','3D')
);
#34876=(
GEOMETRIC_REPRESENTATION_CONTEXT(3)
GLOBAL_UNCERTAINTY_ASSIGNED_CONTEXT((#34841))
GLOBAL_UNIT_ASSIGNED_CONTEXT((#34877,#34878,#34879))
REPRESENTATION_CONTEXT('','3D')
);
#34877=(
LENGTH_UNIT()
NAMED_UNIT(*)
SI_UNIT($,.METRE.)
);
#34878=(
NAMED_UNIT(*)
PLANE_ANGLE_UNIT()
SI_UNIT($,.RADIAN.)
);
#34879=(
NAMED_UNIT(*)
SI_UNIT($,.STERADIAN.)
SOLID_ANGLE_UNIT()
);
#34888=SHAPE_DEFINITION_REPRESENTATION(#34922,#34992);
#34922=PRODUCT_DEFINITION_SHAPE('',$,#35027);
#34992=SHAPE_REPRESENTATION('',(#20809),#34850);
#35018=PRODUCT_DEFINITION_CONTEXT('part definition',#35122,'design');
#35027=PRODUCT_DEFINITION('Socket Screw 1','Socket Screw 1',#35061,#35018);
#35061=PRODUCT_DEFINITION_FORMATION('',$,#35132);
#35122=APPLICATION_CONTEXT('Managed model based 3d engineering');
#35123=PRODUCT_CONTEXT('part definition',#35122,'mechanical');
#35132=PRODUCT('Socket Screw 1','Socket Screw 1',
'LEGAL AND USAGE DISCLAIMER: this Data/Model is provided \X2\201C\X0\A
S IS\X2\201D\X0\ for informational and representational only. It is a 
geometric approximation and is NOT engineered, certified, or guarantee
d for dimensional accuracy, exact tolerances, or production-level prec
ision. Vendor disclaims all implied warranties including fitness for a
 particular purpose. DO NOT USE FOR DIRECT PHYSICAL MANUFACTURING, AUT
OMATED PRODUCTION, OR SAFETY-CRITICAL SYSTEMS without independent engi
neering verification and resolution of any design discrepancies.',(#35123));
#35164=PRESENTATION_STYLE_ASSIGNMENT((#35173));
#35173=SURFACE_STYLE_USAGE(.BOTH.,#35182);
#35182=SURFACE_SIDE_STYLE('',(#35191));
#35191=SURFACE_STYLE_FILL_AREA(#35200);
#35200=FILL_AREA_STYLE('Plastic - Matte (White)',(#35209));
#35209=FILL_AREA_STYLE_COLOUR('Plastic - Matte (White)',#35218);
#35218=COLOUR_RGB('Plastic - Matte (White)',0.964705882352941,0.964705882352941,
0.952941176470588);
ENDSEC;
END-ISO-10303-21;
